ISO-10303-21;
HEADER;
/* Generated by software containing ST-Developer
 * from STEP Tools, Inc. (www.steptools.com) 
 */

FILE_DESCRIPTION(
/* description */ ('Bin tilter linkage'),
/* implementation_level */ '2;1');

FILE_NAME(
/* name */ 'M4 short cap screw (18).step',
/* time_stamp */ '2026-10-28T03:26:24-07:00',
/* author */ (''),
/* organization */ (''),
/* preprocessor_version */ 'ST-DEVELOPER v20.2',
/* originating_system */ 'Autodesk Translation Framework v15.17.0.0',
/* authorisation */ '');

FILE_SCHEMA (('AUTOMOTIVE_DESIGN { 1 0 10303 214 3 1 1 }'));
ENDSEC;

DATA;
#10=MECHANICAL_DESIGN_GEOMETRIC_PRESENTATION_REPRESENTATION('',(#917),#23728);
#705=SHAPE_REPRESENTATION_RELATIONSHIP('SRR','None',#24171,#811);
#811=ADVANCED_BREP_SHAPE_REPRESENTATION('',(#1030),#23671);
#917=STYLED_ITEM('',(#24772),#1030);
#1030=MANIFOLD_SOLID_BREP('Body1',#12448);
#1342=FACE_BOUND('',#3334,.T.);
#1689=PLANE('',#14571);
#1690=PLANE('',#14576);
#1691=PLANE('',#14579);
#2301=FACE_OUTER_BOUND('',#3333,.T.);
#2302=FACE_OUTER_BOUND('',#3335,.T.);
#2303=FACE_OUTER_BOUND('',#3336,.T.);
#2304=FACE_OUTER_BOUND('',#3337,.T.);
#2305=FACE_OUTER_BOUND('',#3338,.T.);
#3333=EDGE_LOOP('',(#9937));
#3334=EDGE_LOOP('',(#9938));
#3335=EDGE_LOOP('',(#9939,#9940,#9941,#9942));
#3336=EDGE_LOOP('',(#9943));
#3337=EDGE_LOOP('',(#9944,#9945,#9946,#9947));
#3338=EDGE_LOOP('',(#9948));
#4207=LINE('',#21525,#4882);
#4208=LINE('',#21531,#4883);
#4882=VECTOR('',#17630,0.350000000000001);
#4883=VECTOR('',#17639,0.199999999999999);
#5623=CIRCLE('',#14572,0.350000000000001);
#5624=CIRCLE('',#14573,0.199999999999999);
#5625=CIRCLE('',#14575,0.350000000000001);
#5626=CIRCLE('',#14578,0.199999999999999);
#6477=VERTEX_POINT('',#21519);
#6478=VERTEX_POINT('',#21521);
#6479=VERTEX_POINT('',#21524);
#6480=VERTEX_POINT('',#21529);
#7708=EDGE_CURVE('',#6477,#6477,#5623,.T.);
#7709=EDGE_CURVE('',#6478,#6478,#5624,.T.);
#7710=EDGE_CURVE('',#6477,#6479,#4207,.T.);
#7711=EDGE_CURVE('',#6479,#6479,#5625,.T.);
#7712=EDGE_CURVE('',#6480,#6480,#5626,.T.);
#7713=EDGE_CURVE('',#6480,#6478,#4208,.T.);
#9937=ORIENTED_EDGE('',*,*,#7708,.T.);
#9938=ORIENTED_EDGE('',*,*,#7709,.F.);
#9939=ORIENTED_EDGE('',*,*,#7708,.F.);
#9940=ORIENTED_EDGE('',*,*,#7710,.T.);
#9941=ORIENTED_EDGE('',*,*,#7711,.T.);
#9942=ORIENTED_EDGE('',*,*,#7710,.F.);
#9943=ORIENTED_EDGE('',*,*,#7711,.F.);
#9944=ORIENTED_EDGE('',*,*,#7712,.F.);
#9945=ORIENTED_EDGE('',*,*,#7713,.T.);
#9946=ORIENTED_EDGE('',*,*,#7709,.T.);
#9947=ORIENTED_EDGE('',*,*,#7713,.F.);
#9948=ORIENTED_EDGE('',*,*,#7712,.T.);
#11477=CYLINDRICAL_SURFACE('',#14574,0.350000000000001);
#11478=CYLINDRICAL_SURFACE('',#14577,0.199999999999999);
#12026=ADVANCED_FACE('',(#2301,#1342),#1689,.T.);
#12027=ADVANCED_FACE('',(#2302),#11477,.T.);
#12028=ADVANCED_FACE('',(#2303),#1690,.F.);
#12029=ADVANCED_FACE('',(#2304),#11478,.T.);
#12030=ADVANCED_FACE('',(#2305),#1691,.T.);
#12448=CLOSED_SHELL('',(#12026,#12027,#12028,#12029,#12030));
#14570=AXIS2_PLACEMENT_3D('',#21517,#17620,#17621);
#14571=AXIS2_PLACEMENT_3D('',#21518,#17622,#17623);
#14572=AXIS2_PLACEMENT_3D('',#21520,#17624,#17625);
#14573=AXIS2_PLACEMENT_3D('',#21522,#17626,#17627);
#14574=AXIS2_PLACEMENT_3D('',#21523,#17628,#17629);
#14575=AXIS2_PLACEMENT_3D('',#21526,#17631,#17632);
#14576=AXIS2_PLACEMENT_3D('',#21527,#17633,#17634);
#14577=AXIS2_PLACEMENT_3D('',#21528,#17635,#17636);
#14578=AXIS2_PLACEMENT_3D('',#21530,#17637,#17638);
#14579=AXIS2_PLACEMENT_3D('',#21532,#17640,#17641);
#17620=DIRECTION('axis',(0.,0.,1.));
#17621=DIRECTION('refdir',(1.,0.,0.));
#17622=DIRECTION('center_axis',(0.,1.,0.));
#17623=DIRECTION('ref_axis',(1.,0.,0.));
#17624=DIRECTION('center_axis',(0.,1.,0.));
#17625=DIRECTION('ref_axis',(1.,0.,0.));
#17626=DIRECTION('center_axis',(0.,1.,0.));
#17627=DIRECTION('ref_axis',(1.,0.,0.));
#17628=DIRECTION('center_axis',(0.,1.,0.));
#17629=DIRECTION('ref_axis',(1.,0.,0.));
#17630=DIRECTION('',(0.,-1.,0.));
#17631=DIRECTION('center_axis',(0.,1.,0.));
#17632=DIRECTION('ref_axis',(1.,0.,0.));
#17633=DIRECTION('center_axis',(0.,1.,0.));
#17634=DIRECTION('ref_axis',(1.,0.,0.));
#17635=DIRECTION('center_axis',(0.,1.,0.));
#17636=DIRECTION('ref_axis',(1.,0.,0.));
#17637=DIRECTION('center_axis',(0.,1.,0.));
#17638=DIRECTION('ref_axis',(1.,0.,0.));
#17639=DIRECTION('',(0.,-1.,0.));
#17640=DIRECTION('center_axis',(0.,1.,0.));
#17641=DIRECTION('ref_axis',(1.,0.,0.));
#21517=CARTESIAN_POINT('',(0.,0.,0.));
#21518=CARTESIAN_POINT('Origin',(16.6918524548049,-0.8,13.6918524548049));
#21519=CARTESIAN_POINT('',(16.3418524548049,-0.8,13.6918524548049));
#21520=CARTESIAN_POINT('Origin',(16.6918524548049,-0.8,13.6918524548049));
#21521=CARTESIAN_POINT('',(16.4918524548049,-0.8,13.6918524548049));
#21522=CARTESIAN_POINT('Origin',(16.6918524548049,-0.8,13.6918524548049));
#21523=CARTESIAN_POINT('Origin',(16.6918524548049,-1.2,13.6918524548049));
#21524=CARTESIAN_POINT('',(16.3418524548049,-1.2,13.6918524548049));
#21525=CARTESIAN_POINT('',(16.3418524548049,-1.2,13.6918524548049));
#21526=CARTESIAN_POINT('Origin',(16.6918524548049,-1.2,13.6918524548049));
#21527=CARTESIAN_POINT('Origin',(16.6918524548049,-1.2,13.6918524548049));
#21528=CARTESIAN_POINT('Origin',(16.6918524548049,-0.8,13.6918524548049));
#21529=CARTESIAN_POINT('',(16.4918524548049,-0.1,13.6918524548049));
#21530=CARTESIAN_POINT('Origin',(16.6918524548049,-0.1,13.6918524548049));
#21531=CARTESIAN_POINT('',(16.4918524548049,-0.8,13.6918524548049));
#21532=CARTESIAN_POINT('Origin',(16.6918524548049,-0.1,13.6918524548049));
#23554=UNCERTAINTY_MEASURE_WITH_UNIT(LENGTH_MEASURE(0.001),#23729,
'DISTANCE_ACCURACY_VALUE',
'Maximum model space distance between geometric entities at asserted c
onnectivities');
#23611=UNCERTAINTY_MEASURE_WITH_UNIT(LENGTH_MEASURE(0.001),#23729,
'DISTANCE_ACCURACY_VALUE',
'Maximum model space distance between geometric entities at asserted c
onnectivities');
#23671=(
GEOMETRIC_REPRESENTATION_CONTEXT(3)
GLOBAL_UNCERTAINTY_ASSIGNED_CONTEXT((#23554))
GLOBAL_UNIT_ASSIGNED_CONTEXT((#23729,#23731,#23732))
REPRESENTATION_CONTEXT('','3D')
);
#23728=(
GEOMETRIC_REPRESENTATION_CONTEXT(3)
GLOBAL_UNCERTAINTY_ASSIGNED_CONTEXT((#23611))
GLOBAL_UNIT_ASSIGNED_CONTEXT((#23729,#23731,#23732))
REPRESENTATION_CONTEXT('','3D')
);
#23729=(
LENGTH_UNIT()
NAMED_UNIT(*)
SI_UNIT(.CENTI.,.METRE.)
);
#23731=(
NAMED_UNIT(*)
PLANE_ANGLE_UNIT()
SI_UNIT($,.RADIAN.)
);
#23732=(
NAMED_UNIT(*)
SI_UNIT($,.STERADIAN.)
SOLID_ANGLE_UNIT()
);
#23792=SHAPE_DEFINITION_REPRESENTATION(#23908,#24171);
#23908=PRODUCT_DEFINITION_SHAPE('',$,#24288);
#24171=SHAPE_REPRESENTATION('',(#14570),#23671);
#24228=PRODUCT_DEFINITION_CONTEXT('part definition',#24578,'design');
#24288=PRODUCT_DEFINITION('M4 short cap screw (18)',
'M4 short cap screw (18)',#24404,#24228);
#24404=PRODUCT_DEFINITION_FORMATION('',$,#24639);
#24578=APPLICATION_CONTEXT(
'Core Data for Automotive Mechanical Design Process');
#24579=PRODUCT_CONTEXT('part definition',#24578,'mechanical');
#24639=PRODUCT('M4 short cap screw (18)','M4 short cap screw (18)',
'M4 short cap screw (18)',(#24579));
#24766=COLOUR_RGB('Black',0.12,0.14,0.17);
#24767=FILL_AREA_STYLE_COLOUR('',#24766);
#24768=FILL_AREA_STYLE('',(#24767));
#24769=SURFACE_STYLE_FILL_AREA(#24768);
#24770=SURFACE_SIDE_STYLE('',(#24769));
#24771=SURFACE_STYLE_USAGE(.BOTH.,#24770);
#24772=PRESENTATION_STYLE_ASSIGNMENT((#24771));
ENDSEC;
END-ISO-10303-21;
